ISO-10303-21;
HEADER;
/* Generated by software containing ST-Developer
 * from STEP Tools, Inc. (www.steptools.com) 
 */

FILE_DESCRIPTION(
/* description */ ('Spring compression tester'),
/* implementation_level */ '2;1');

FILE_NAME(
/* name */ 'Cap Screw - M4x16.step',
/* time_stamp */ '2026-10-28T03:24:11-07:00',
/* author */ (''),
/* organization */ (''),
/* preprocessor_version */ 'ST-DEVELOPER v20.2',
/* originating_system */ 'Autodesk Translation Framework v15.17.0.0',
/* authorisation */ '');

FILE_SCHEMA (('AUTOMOTIVE_DESIGN { 1 0 10303 214 3 1 1 }'));
ENDSEC;

DATA;
#10=MECHANICAL_DESIGN_GEOMETRIC_PRESENTATION_REPRESENTATION('',(#1168),#43521);
#936=ORIENTED_CLOSED_SHELL('',*,#18611,.F.);
#943=BREP_WITH_VOIDS('Body1',#18610,(#936));
#974=CONICAL_SURFACE('',#20767,0.325,0.785398163397448);
#975=CONICAL_SURFACE('',#20771,0.335,0.785398163397448);
#976=CONICAL_SURFACE('',#20775,0.21,0.463647609000806);
#977=CONICAL_SURFACE('',#20779,0.18,0.785398163397448);
#1033=SHAPE_REPRESENTATION_RELATIONSHIP('SRR','None',#43849,#1093);
#1093=ADVANCED_BREP_SHAPE_REPRESENTATION('',(#943),#43509);
#1168=STYLED_ITEM('',(#44209),#943);
#1564=FACE_BOUND('',#4351,.T.);
#2099=PLANE('',#20765);
#2100=PLANE('',#20773);
#2101=PLANE('',#20781);
#2102=PLANE('',#20782);
#2103=PLANE('',#20783);
#2104=PLANE('',#20784);
#2105=PLANE('',#20785);
#2106=PLANE('',#20786);
#2107=PLANE('',#20787);
#2108=PLANE('',#20788);
#2109=PLANE('',#20789);
#2982=FACE_OUTER_BOUND('',#4346,.T.);
#2983=FACE_OUTER_BOUND('',#4347,.T.);
#2984=FACE_OUTER_BOUND('',#4348,.T.);
#2985=FACE_OUTER_BOUND('',#4349,.T.);
#2986=FACE_OUTER_BOUND('',#4350,.T.);
#2987=FACE_OUTER_BOUND('',#4352,.T.);
#2988=FACE_OUTER_BOUND('',#4353,.T.);
#2989=FACE_OUTER_BOUND('',#4354,.T.);
#2990=FACE_OUTER_BOUND('',#4355,.T.);
#2991=FACE_OUTER_BOUND('',#4356,.T.);
#2992=FACE_OUTER_BOUND('',#4357,.T.);
#2993=FACE_OUTER_BOUND('',#4358,.T.);
#2994=FACE_OUTER_BOUND('',#4359,.T.);
#2995=FACE_OUTER_BOUND('',#4360,.T.);
#2996=FACE_OUTER_BOUND('',#4361,.T.);
#2997=FACE_OUTER_BOUND('',#4362,.T.);
#2998=FACE_OUTER_BOUND('',#4363,.T.);
#4346=EDGE_LOOP('',(#15909));
#4347=EDGE_LOOP('',(#15910,#15911,#15912,#15913));
#4348=EDGE_LOOP('',(#15914,#15915,#15916,#15917));
#4349=EDGE_LOOP('',(#15918,#15919,#15920,#15921));
#4350=EDGE_LOOP('',(#15922));
#4351=EDGE_LOOP('',(#15923));
#4352=EDGE_LOOP('',(#15924,#15925,#15926,#15927));
#4353=EDGE_LOOP('',(#15928,#15929,#15930,#15931));
#4354=EDGE_LOOP('',(#15932,#15933,#15934,#15935));
#4355=EDGE_LOOP('',(#15936));
#4356=EDGE_LOOP('',(#15937,#15938,#15939,#15940));
#4357=EDGE_LOOP('',(#15941,#15942,#15943,#15944));
#4358=EDGE_LOOP('',(#15945,#15946,#15947,#15948));
#4359=EDGE_LOOP('',(#15949,#15950,#15951,#15952));
#4360=EDGE_LOOP('',(#15953,#15954,#15955,#15956));
#4361=EDGE_LOOP('',(#15957,#15958,#15959,#15960));
#4362=EDGE_LOOP('',(#15961,#15962,#15963,#15964,#15965,#15966));
#4363=EDGE_LOOP('',(#15967,#15968,#15969,#15970,#15971,#15972));
#5774=LINE('',#33086,#7206);
#5775=LINE('',#33090,#7207);
#5776=LINE('',#33094,#7208);
#5777=LINE('',#33101,#7209);
#5778=LINE('',#33105,#7210);
#5779=LINE('',#33109,#7211);
#5780=LINE('',#33114,#7212);
#5781=LINE('',#33116,#7213);
#5782=LINE('',#33118,#7214);
#5783=LINE('',#33119,#7215);
#5784=LINE('',#33122,#7216);
#5785=LINE('',#33124,#7217);
#5786=LINE('',#33125,#7218);
#5787=LINE('',#33128,#7219);
#5788=LINE('',#33130,#7220);
#5789=LINE('',#33131,#7221);
#5790=LINE('',#33134,#7222);
#5791=LINE('',#33136,#7223);
#5792=LINE('',#33137,#7224);
#5793=LINE('',#33140,#7225);
#5794=LINE('',#33142,#7226);
#5795=LINE('',#33143,#7227);
#5796=LINE('',#33145,#7228);
#5797=LINE('',#33146,#7229);
#7206=VECTOR('',#25334,0.325);
#7207=VECTOR('',#25339,0.35);
#7208=VECTOR('',#25344,0.335);
#7209=VECTOR('',#25353,0.21);
#7210=VECTOR('',#25358,0.2);
#7211=VECTOR('',#25363,0.18);
#7212=VECTOR('',#25368,1.);
#7213=VECTOR('',#25369,1.);
#7214=VECTOR('',#25370,1.);
#7215=VECTOR('',#25371,1.);
#7216=VECTOR('',#25374,1.);
#7217=VECTOR('',#25375,1.);
#7218=VECTOR('',#25376,1.);
#7219=VECTOR('',#25379,1.);
#7220=VECTOR('',#25380,1.);
#7221=VECTOR('',#25381,1.);
#7222=VECTOR('',#25384,1.);
#7223=VECTOR('',#25385,1.);
#7224=VECTOR('',#25386,1.);
#7225=VECTOR('',#25389,1.);
#7226=VECTOR('',#25390,1.);
#7227=VECTOR('',#25391,1.);
#7228=VECTOR('',#25394,1.);
#7229=VECTOR('',#25395,1.);
#8071=CIRCLE('',#20766,0.3);
#8072=CIRCLE('',#20768,0.35);
#8073=CIRCLE('',#20770,0.35);
#8074=CIRCLE('',#20772,0.32);
#8075=CIRCLE('',#20774,0.22);
#8076=CIRCLE('',#20776,0.1954);
#8077=CIRCLE('',#20778,0.1954);
#8078=CIRCLE('',#20780,0.16);
#9377=VERTEX_POINT('',#33081);
#9378=VERTEX_POINT('',#33084);
#9379=VERTEX_POINT('',#33088);
#9380=VERTEX_POINT('',#33092);
#9381=VERTEX_POINT('',#33096);
#9382=VERTEX_POINT('',#33099);
#9383=VERTEX_POINT('',#33103);
#9384=VERTEX_POINT('',#33107);
#9385=VERTEX_POINT('',#33112);
#9386=VERTEX_POINT('',#33113);
#9387=VERTEX_POINT('',#33115);
#9388=VERTEX_POINT('',#33117);
#9389=VERTEX_POINT('',#33121);
#9390=VERTEX_POINT('',#33123);
#9391=VERTEX_POINT('',#33127);
#9392=VERTEX_POINT('',#33129);
#9393=VERTEX_POINT('',#33133);
#9394=VERTEX_POINT('',#33135);
#9395=VERTEX_POINT('',#33139);
#9396=VERTEX_POINT('',#33141);
#11619=EDGE_CURVE('',#9377,#9377,#8071,.T.);
#11620=EDGE_CURVE('',#9378,#9378,#8072,.T.);
#11621=EDGE_CURVE('',#9378,#9377,#5774,.T.);
#11622=EDGE_CURVE('',#9379,#9379,#8073,.T.);
#11623=EDGE_CURVE('',#9379,#9378,#5775,.T.);
#11624=EDGE_CURVE('',#9380,#9380,#8074,.T.);
#11625=EDGE_CURVE('',#9380,#9379,#5776,.T.);
#11626=EDGE_CURVE('',#9381,#9381,#8075,.T.);
#11627=EDGE_CURVE('',#9382,#9382,#8076,.F.);
#11628=EDGE_CURVE('',#9382,#9381,#5777,.T.);
#11629=EDGE_CURVE('',#9383,#9383,#8077,.F.);
#11630=EDGE_CURVE('',#9383,#9382,#5778,.T.);
#11631=EDGE_CURVE('',#9384,#9384,#8078,.T.);
#11632=EDGE_CURVE('',#9384,#9383,#5779,.T.);
#11633=EDGE_CURVE('',#9385,#9386,#5780,.T.);
#11634=EDGE_CURVE('',#9386,#9387,#5781,.T.);
#11635=EDGE_CURVE('',#9387,#9388,#5782,.T.);
#11636=EDGE_CURVE('',#9385,#9388,#5783,.T.);
#11637=EDGE_CURVE('',#9386,#9389,#5784,.T.);
#11638=EDGE_CURVE('',#9389,#9390,#5785,.T.);
#11639=EDGE_CURVE('',#9390,#9387,#5786,.T.);
#11640=EDGE_CURVE('',#9389,#9391,#5787,.T.);
#11641=EDGE_CURVE('',#9391,#9392,#5788,.T.);
#11642=EDGE_CURVE('',#9392,#9390,#5789,.T.);
#11643=EDGE_CURVE('',#9391,#9393,#5790,.T.);
#11644=EDGE_CURVE('',#9393,#9394,#5791,.T.);
#11645=EDGE_CURVE('',#9394,#9392,#5792,.T.);
#11646=EDGE_CURVE('',#9393,#9395,#5793,.T.);
#11647=EDGE_CURVE('',#9395,#9396,#5794,.T.);
#11648=EDGE_CURVE('',#9396,#9394,#5795,.T.);
#11649=EDGE_CURVE('',#9395,#9385,#5796,.T.);
#11650=EDGE_CURVE('',#9388,#9396,#5797,.T.);
#15909=ORIENTED_EDGE('',*,*,#11619,.F.);
#15910=ORIENTED_EDGE('',*,*,#11620,.F.);
#15911=ORIENTED_EDGE('',*,*,#11621,.T.);
#15912=ORIENTED_EDGE('',*,*,#11619,.T.);
#15913=ORIENTED_EDGE('',*,*,#11621,.F.);
#15914=ORIENTED_EDGE('',*,*,#11622,.F.);
#15915=ORIENTED_EDGE('',*,*,#11623,.T.);
#15916=ORIENTED_EDGE('',*,*,#11620,.T.);
#15917=ORIENTED_EDGE('',*,*,#11623,.F.);
#15918=ORIENTED_EDGE('',*,*,#11624,.F.);
#15919=ORIENTED_EDGE('',*,*,#11625,.T.);
#15920=ORIENTED_EDGE('',*,*,#11622,.T.);
#15921=ORIENTED_EDGE('',*,*,#11625,.F.);
#15922=ORIENTED_EDGE('',*,*,#11624,.T.);
#15923=ORIENTED_EDGE('',*,*,#11626,.F.);
#15924=ORIENTED_EDGE('',*,*,#11627,.F.);
#15925=ORIENTED_EDGE('',*,*,#11628,.T.);
#15926=ORIENTED_EDGE('',*,*,#11626,.T.);
#15927=ORIENTED_EDGE('',*,*,#11628,.F.);
#15928=ORIENTED_EDGE('',*,*,#11629,.F.);
#15929=ORIENTED_EDGE('',*,*,#11630,.T.);
#15930=ORIENTED_EDGE('',*,*,#11627,.T.);
#15931=ORIENTED_EDGE('',*,*,#11630,.F.);
#15932=ORIENTED_EDGE('',*,*,#11631,.F.);
#15933=ORIENTED_EDGE('',*,*,#11632,.T.);
#15934=ORIENTED_EDGE('',*,*,#11629,.T.);
#15935=ORIENTED_EDGE('',*,*,#11632,.F.);
#15936=ORIENTED_EDGE('',*,*,#11631,.T.);
#15937=ORIENTED_EDGE('',*,*,#11633,.T.);
#15938=ORIENTED_EDGE('',*,*,#11634,.T.);
#15939=ORIENTED_EDGE('',*,*,#11635,.T.);
#15940=ORIENTED_EDGE('',*,*,#11636,.F.);
#15941=ORIENTED_EDGE('',*,*,#11637,.T.);
#15942=ORIENTED_EDGE('',*,*,#11638,.T.);
#15943=ORIENTED_EDGE('',*,*,#11639,.T.);
#15944=ORIENTED_EDGE('',*,*,#11634,.F.);
#15945=ORIENTED_EDGE('',*,*,#11640,.T.);
#15946=ORIENTED_EDGE('',*,*,#11641,.T.);
#15947=ORIENTED_EDGE('',*,*,#11642,.T.);
#15948=ORIENTED_EDGE('',*,*,#11638,.F.);
#15949=ORIENTED_EDGE('',*,*,#11643,.T.);
#15950=ORIENTED_EDGE('',*,*,#11644,.T.);
#15951=ORIENTED_EDGE('',*,*,#11645,.T.);
#15952=ORIENTED_EDGE('',*,*,#11641,.F.);
#15953=ORIENTED_EDGE('',*,*,#11646,.T.);
#15954=ORIENTED_EDGE('',*,*,#11647,.T.);
#15955=ORIENTED_EDGE('',*,*,#11648,.T.);
#15956=ORIENTED_EDGE('',*,*,#11644,.F.);
#15957=ORIENTED_EDGE('',*,*,#11649,.T.);
#15958=ORIENTED_EDGE('',*,*,#11636,.T.);
#15959=ORIENTED_EDGE('',*,*,#11650,.T.);
#15960=ORIENTED_EDGE('',*,*,#11647,.F.);
#15961=ORIENTED_EDGE('',*,*,#11649,.F.);
#15962=ORIENTED_EDGE('',*,*,#11646,.F.);
#15963=ORIENTED_EDGE('',*,*,#11643,.F.);
#15964=ORIENTED_EDGE('',*,*,#11640,.F.);
#15965=ORIENTED_EDGE('',*,*,#11637,.F.);
#15966=ORIENTED_EDGE('',*,*,#11633,.F.);
#15967=ORIENTED_EDGE('',*,*,#11650,.F.);
#15968=ORIENTED_EDGE('',*,*,#11635,.F.);
#15969=ORIENTED_EDGE('',*,*,#11639,.F.);
#15970=ORIENTED_EDGE('',*,*,#11642,.F.);
#15971=ORIENTED_EDGE('',*,*,#11645,.F.);
#15972=ORIENTED_EDGE('',*,*,#11648,.F.);
#17342=CYLINDRICAL_SURFACE('',#20769,0.35);
#17343=CYLINDRICAL_SURFACE('',#20777,0.1954);
#18306=ADVANCED_FACE('',(#2982),#2099,.T.);
#18307=ADVANCED_FACE('',(#2983),#974,.T.);
#18308=ADVANCED_FACE('',(#2984),#17342,.T.);
#18309=ADVANCED_FACE('',(#2985),#975,.T.);
#18310=ADVANCED_FACE('',(#2986,#1564),#2100,.T.);
#18311=ADVANCED_FACE('',(#2987),#976,.T.);
#18312=ADVANCED_FACE('',(#2988),#17343,.T.);
#18313=ADVANCED_FACE('',(#2989),#977,.T.);
#18314=ADVANCED_FACE('',(#2990),#2101,.T.);
#18315=ADVANCED_FACE('',(#2991),#2102,.F.);
#18316=ADVANCED_FACE('',(#2992),#2103,.F.);
#18317=ADVANCED_FACE('',(#2993),#2104,.F.);
#18318=ADVANCED_FACE('',(#2994),#2105,.F.);
#18319=ADVANCED_FACE('',(#2995),#2106,.F.);
#18320=ADVANCED_FACE('',(#2996),#2107,.F.);
#18321=ADVANCED_FACE('',(#2997),#2108,.F.);
#18322=ADVANCED_FACE('',(#2998),#2109,.F.);
#18610=CLOSED_SHELL('',(#18306,#18307,#18308,#18309,#18310,#18311,#18312,
#18313,#18314));
#18611=CLOSED_SHELL('',(#18315,#18316,#18317,#18318,#18319,#18320,#18321,
#18322));
#20764=AXIS2_PLACEMENT_3D('',#33079,#25324,#25325);
#20765=AXIS2_PLACEMENT_3D('',#33080,#25326,#25327);
#20766=AXIS2_PLACEMENT_3D('',#33082,#25328,#25329);
#20767=AXIS2_PLACEMENT_3D('',#33083,#25330,#25331);
#20768=AXIS2_PLACEMENT_3D('',#33085,#25332,#25333);
#20769=AXIS2_PLACEMENT_3D('',#33087,#25335,#25336);
#20770=AXIS2_PLACEMENT_3D('',#33089,#25337,#25338);
#20771=AXIS2_PLACEMENT_3D('',#33091,#25340,#25341);
#20772=AXIS2_PLACEMENT_3D('',#33093,#25342,#25343);
#20773=AXIS2_PLACEMENT_3D('',#33095,#25345,#25346);
#20774=AXIS2_PLACEMENT_3D('',#33097,#25347,#25348);
#20775=AXIS2_PLACEMENT_3D('',#33098,#25349,#25350);
#20776=AXIS2_PLACEMENT_3D('',#33100,#25351,#25352);
#20777=AXIS2_PLACEMENT_3D('',#33102,#25354,#25355);
#20778=AXIS2_PLACEMENT_3D('',#33104,#25356,#25357);
#20779=AXIS2_PLACEMENT_3D('',#33106,#25359,#25360);
#20780=AXIS2_PLACEMENT_3D('',#33108,#25361,#25362);
#20781=AXIS2_PLACEMENT_3D('',#33110,#25364,#25365);
#20782=AXIS2_PLACEMENT_3D('',#33111,#25366,#25367);
#20783=AXIS2_PLACEMENT_3D('',#33120,#25372,#25373);
#20784=AXIS2_PLACEMENT_3D('',#33126,#25377,#25378);
#20785=AXIS2_PLACEMENT_3D('',#33132,#25382,#25383);
#20786=AXIS2_PLACEMENT_3D('',#33138,#25387,#25388);
#20787=AXIS2_PLACEMENT_3D('',#33144,#25392,#25393);
#20788=AXIS2_PLACEMENT_3D('',#33147,#25396,#25397);
#20789=AXIS2_PLACEMENT_3D('',#33148,#25398,#25399);
#25324=DIRECTION('axis',(0.,0.,1.));
#25325=DIRECTION('refdir',(1.,0.,0.));
#25326=DIRECTION('center_axis',(0.,1.,0.));
#25327=DIRECTION('ref_axis',(0.,0.,1.));
#25328=DIRECTION('center_axis',(0.,-1.,0.));
#25329=DIRECTION('ref_axis',(1.,0.,0.));
#25330=DIRECTION('center_axis',(0.,-1.,0.));
#25331=DIRECTION('ref_axis',(1.,0.,0.));
#25332=DIRECTION('center_axis',(0.,-1.,0.));
#25333=DIRECTION('ref_axis',(1.,0.,0.));
#25334=DIRECTION('',(0.707106781186547,0.707106781186548,8.65956056235493E-17));
#25335=DIRECTION('center_axis',(0.,-1.,0.));
#25336=DIRECTION('ref_axis',(1.,0.,0.));
#25337=DIRECTION('center_axis',(0.,-1.,0.));
#25338=DIRECTION('ref_axis',(1.,0.,0.));
#25339=DIRECTION('',(0.,1.,0.));
#25340=DIRECTION('center_axis',(0.,1.,0.));
#25341=DIRECTION('ref_axis',(1.,0.,0.));
#25342=DIRECTION('center_axis',(0.,-1.,0.));
#25343=DIRECTION('ref_axis',(1.,0.,0.));
#25344=DIRECTION('',(-0.707106781186547,0.707106781186548,-8.65956056235493E-17));
#25345=DIRECTION('center_axis',(0.,-1.,0.));
#25346=DIRECTION('ref_axis',(0.,0.,-1.));
#25347=DIRECTION('center_axis',(0.,-1.,0.));
#25348=DIRECTION('ref_axis',(1.,0.,0.));
#25349=DIRECTION('center_axis',(0.,1.,0.));
#25350=DIRECTION('ref_axis',(1.,0.,0.));
#25351=DIRECTION('center_axis',(0.,1.,0.));
#25352=DIRECTION('ref_axis',(1.,0.,0.));
#25353=DIRECTION('',(-0.447213595499958,0.894427190999916,-5.47678698264203E-17));
#25354=DIRECTION('center_axis',(0.,-1.,0.));
#25355=DIRECTION('ref_axis',(1.,0.,0.));
#25356=DIRECTION('center_axis',(0.,1.,0.));
#25357=DIRECTION('ref_axis',(1.,0.,0.));
#25358=DIRECTION('',(0.,1.,0.));
#25359=DIRECTION('center_axis',(0.,1.,0.));
#25360=DIRECTION('ref_axis',(1.,0.,0.));
#25361=DIRECTION('center_axis',(0.,-1.,0.));
#25362=DIRECTION('ref_axis',(1.,0.,0.));
#25363=DIRECTION('',(-0.707106781186547,0.707106781186548,-8.65956056235493E-17));
#25364=DIRECTION('center_axis',(0.,-1.,0.));
#25365=DIRECTION('ref_axis',(0.,0.,-1.));
#25366=DIRECTION('center_axis',(0.866025403784439,0.,-0.5));
#25367=DIRECTION('ref_axis',(0.5,0.,0.866025403784439));
#25368=DIRECTION('',(-0.5,0.,-0.866025403784439));
#25369=DIRECTION('',(0.,-1.,0.));
#25370=DIRECTION('',(0.5,0.,0.866025403784439));
#25371=DIRECTION('',(0.,-1.,0.));
#25372=DIRECTION('center_axis',(1.60246890531964E-16,0.,-1.));
#25373=DIRECTION('ref_axis',(1.,0.,1.60246890531964E-16));
#25374=DIRECTION('',(-1.,0.,-1.60246890531964E-16));
#25375=DIRECTION('',(0.,-1.,0.));
#25376=DIRECTION('',(1.,0.,1.60246890531964E-16));
#25377=DIRECTION('center_axis',(-0.866025403784439,0.,-0.5));
#25378=DIRECTION('ref_axis',(0.5,0.,-0.866025403784439));
#25379=DIRECTION('',(-0.5,0.,0.866025403784439));
#25380=DIRECTION('',(0.,-1.,0.));
#25381=DIRECTION('',(0.5,0.,-0.866025403784439));
#25382=DIRECTION('center_axis',(-0.866025403784439,0.,0.5));
#25383=DIRECTION('ref_axis',(-0.5,0.,-0.866025403784439));
#25384=DIRECTION('',(0.5,0.,0.866025403784439));
#25385=DIRECTION('',(0.,-1.,0.));
#25386=DIRECTION('',(-0.5,0.,-0.866025403784439));
#25387=DIRECTION('center_axis',(-1.60246890531964E-16,0.,1.));
#25388=DIRECTION('ref_axis',(-1.,0.,-1.60246890531964E-16));
#25389=DIRECTION('',(1.,0.,1.60246890531964E-16));
#25390=DIRECTION('',(0.,-1.,0.));
#25391=DIRECTION('',(-1.,0.,-1.60246890531964E-16));
#25392=DIRECTION('center_axis',(0.866025403784439,0.,0.5));
#25393=DIRECTION('ref_axis',(-0.5,0.,0.866025403784439));
#25394=DIRECTION('',(0.5,0.,-0.866025403784439));
#25395=DIRECTION('',(-0.5,0.,0.866025403784439));
#25396=DIRECTION('center_axis',(0.,1.,0.));
#25397=DIRECTION('ref_axis',(1.,0.,0.));
#25398=DIRECTION('center_axis',(0.,-1.,0.));
#25399=DIRECTION('ref_axis',(0.,0.,-1.));
#33079=CARTESIAN_POINT('',(0.,0.,0.));
#33080=CARTESIAN_POINT('Origin',(0.3,0.4,0.));
#33081=CARTESIAN_POINT('',(-0.3,0.4,-3.67394039744206E-17));
#33082=CARTESIAN_POINT('Origin',(0.,0.4,0.));
#33083=CARTESIAN_POINT('Origin',(0.,0.375,0.));
#33084=CARTESIAN_POINT('',(-0.35,0.35,-4.28626379701573E-17));
#33085=CARTESIAN_POINT('Origin',(0.,0.35,0.));
#33086=CARTESIAN_POINT('',(-0.325,0.375,-3.9801020972289E-17));
#33087=CARTESIAN_POINT('Origin',(0.,0.19,0.));
#33088=CARTESIAN_POINT('',(-0.35,0.03,-4.28626379701574E-17));
#33089=CARTESIAN_POINT('Origin',(0.,0.03,0.));
#33090=CARTESIAN_POINT('',(-0.35,0.19,-4.28626379701574E-17));
#33091=CARTESIAN_POINT('Origin',(0.,0.0149999999999999,0.));
#33092=CARTESIAN_POINT('',(-0.32,-3.29597460435593E-17,-3.91886975727153E-17));
#33093=CARTESIAN_POINT('Origin',(0.,0.,0.));
#33094=CARTESIAN_POINT('',(-0.335,0.0149999999999999,-4.10256677714363E-17));
#33095=CARTESIAN_POINT('Origin',(0.22,0.,0.));
#33096=CARTESIAN_POINT('',(-0.22,-6.93889390390723E-18,-2.69422295812418E-17));
#33097=CARTESIAN_POINT('Origin',(0.,0.,0.));
#33098=CARTESIAN_POINT('Origin',(0.,-0.02,0.));
#33099=CARTESIAN_POINT('',(-0.1954,-0.0492,2.39295984553393E-17));
#33100=CARTESIAN_POINT('Origin',(0.,-0.0492,0.));
#33101=CARTESIAN_POINT('',(-0.21,-0.02,-2.57175827820944E-17));
#33102=CARTESIAN_POINT('Origin',(0.,-0.8,0.));
#33103=CARTESIAN_POINT('',(-0.1954,-1.5646,2.39295984553393E-17));
#33104=CARTESIAN_POINT('Origin',(0.,-1.5646,0.));
#33105=CARTESIAN_POINT('',(-0.1954,-0.8,-2.39295984553393E-17));
#33106=CARTESIAN_POINT('Origin',(0.,-1.58,0.));
#33107=CARTESIAN_POINT('',(-0.16,-1.6,-1.95943487863577E-17));
#33108=CARTESIAN_POINT('Origin',(0.,-1.6,0.));
#33109=CARTESIAN_POINT('',(-0.18,-1.58,-2.20436423846524E-17));
#33110=CARTESIAN_POINT('Origin',(0.,-1.6,0.));
#33111=CARTESIAN_POINT('Origin',(0.0866025403784439,-0.4,-0.15));
#33112=CARTESIAN_POINT('',(0.173205080756888,-0.4,0.));
#33113=CARTESIAN_POINT('',(0.0866025403784439,-0.4,-0.15));
#33114=CARTESIAN_POINT('',(0.173205080756888,-0.4,0.));
#33115=CARTESIAN_POINT('',(0.0866025403784439,-0.64,-0.15));
#33116=CARTESIAN_POINT('',(0.0866025403784439,-0.4,-0.15));
#33117=CARTESIAN_POINT('',(0.173205080756888,-0.64,0.));
#33118=CARTESIAN_POINT('',(0.173205080756888,-0.64,0.));
#33119=CARTESIAN_POINT('',(0.173205080756888,-0.4,0.));
#33120=CARTESIAN_POINT('Origin',(-0.0866025403784438,-0.4,-0.15));
#33121=CARTESIAN_POINT('',(-0.0866025403784438,-0.4,-0.15));
#33122=CARTESIAN_POINT('',(0.0866025403784439,-0.4,-0.15));
#33123=CARTESIAN_POINT('',(-0.0866025403784438,-0.64,-0.15));
#33124=CARTESIAN_POINT('',(-0.0866025403784438,-0.4,-0.15));
#33125=CARTESIAN_POINT('',(0.0866025403784439,-0.64,-0.15));
#33126=CARTESIAN_POINT('Origin',(-0.173205080756888,-0.4,-2.77555756156289E-17));
#33127=CARTESIAN_POINT('',(-0.173205080756888,-0.4,-2.12115047744981E-17));
#33128=CARTESIAN_POINT('',(-0.0866025403784438,-0.4,-0.15));
#33129=CARTESIAN_POINT('',(-0.173205080756888,-0.64,-2.77555756156289E-17));
#33130=CARTESIAN_POINT('',(-0.173205080756888,-0.4,-2.12115047744981E-17));
#33131=CARTESIAN_POINT('',(-0.0866025403784438,-0.64,-0.15));
#33132=CARTESIAN_POINT('Origin',(-0.0866025403784439,-0.4,0.15));
#33133=CARTESIAN_POINT('',(-0.0866025403784439,-0.4,0.15));
#33134=CARTESIAN_POINT('',(-0.173205080756888,-0.4,-2.12115047744981E-17));
#33135=CARTESIAN_POINT('',(-0.0866025403784439,-0.64,0.15));
#33136=CARTESIAN_POINT('',(-0.0866025403784439,-0.4,0.15));
#33137=CARTESIAN_POINT('',(-0.173205080756888,-0.64,-2.12115047744981E-17));
#33138=CARTESIAN_POINT('Origin',(0.0866025403784439,-0.4,0.15));
#33139=CARTESIAN_POINT('',(0.0866025403784439,-0.4,0.15));
#33140=CARTESIAN_POINT('',(-0.0866025403784439,-0.4,0.15));
#33141=CARTESIAN_POINT('',(0.0866025403784439,-0.64,0.15));
#33142=CARTESIAN_POINT('',(0.0866025403784439,-0.4,0.15));
#33143=CARTESIAN_POINT('',(-0.0866025403784439,-0.64,0.15));
#33144=CARTESIAN_POINT('Origin',(0.173205080756888,-0.4,0.));
#33145=CARTESIAN_POINT('',(0.0866025403784439,-0.4,0.15));
#33146=CARTESIAN_POINT('',(0.0866025403784439,-0.64,0.15));
#33147=CARTESIAN_POINT('Origin',(0.,-0.4,-2.77555756156289E-17));
#33148=CARTESIAN_POINT('Origin',(0.,-0.64,-2.77555756156289E-17));
#43441=UNCERTAINTY_MEASURE_WITH_UNIT(LENGTH_MEASURE(0.001),#43522,
'DISTANCE_ACCURACY_VALUE',
'Maximum model space distance between geometric entities at asserted c
onnectivities');
#43453=UNCERTAINTY_MEASURE_WITH_UNIT(LENGTH_MEASURE(0.001),#43522,
'DISTANCE_ACCURACY_VALUE',
'Maximum model space distance between geometric entities at asserted c
onnectivities');
#43509=(
GEOMETRIC_REPRESENTATION_CONTEXT(3)
GLOBAL_UNCERTAINTY_ASSIGNED_CONTEXT((#43441))
GLOBAL_UNIT_ASSIGNED_CONTEXT((#43522,#43524,#43525))
REPRESENTATION_CONTEXT('','3D')
);
#43521=(
GEOMETRIC_REPRESENTATION_CONTEXT(3)
GLOBAL_UNCERTAINTY_ASSIGNED_CONTEXT((#43453))
GLOBAL_UNIT_ASSIGNED_CONTEXT((#43522,#43524,#43525))
REPRESENTATION_CONTEXT('','3D')
);
#43522=(
LENGTH_UNIT()
NAMED_UNIT(*)
SI_UNIT(.CENTI.,.METRE.)
);
#43524=(
NAMED_UNIT(*)
PLANE_ANGLE_UNIT()
SI_UNIT($,.RADIAN.)
);
#43525=(
NAMED_UNIT(*)
SI_UNIT($,.STERADIAN.)
SOLID_ANGLE_UNIT()
);
#43581=SHAPE_DEFINITION_REPRESENTATION(#43660,#43849);
#43660=PRODUCT_DEFINITION_SHAPE('',$,#43917);
#43849=SHAPE_REPRESENTATION('',(#20764),#43509);
#43861=PRODUCT_DEFINITION_CONTEXT('part definition',#44064,'design');
#43917=PRODUCT_DEFINITION('Cap Screw - M4x16','Cap Screw - M4x16',#43984,
#43861);
#43984=PRODUCT_DEFINITION_FORMATION('',$,#44121);
#44064=APPLICATION_CONTEXT(
'Core Data for Automotive Mechanical Design Process');
#44065=PRODUCT_CONTEXT('part definition',#44064,'mechanical');
#44121=PRODUCT('Cap Screw - M4x16','Cap Screw - M4x16',
'Cap Screw - M4x16',(#44065));
#44203=COLOUR_RGB('Black',0.12,0.14,0.17);
#44204=FILL_AREA_STYLE_COLOUR('',#44203);
#44205=FILL_AREA_STYLE('',(#44204));
#44206=SURFACE_STYLE_FILL_AREA(#44205);
#44207=SURFACE_SIDE_STYLE('',(#44206));
#44208=SURFACE_STYLE_USAGE(.BOTH.,#44207);
#44209=PRESENTATION_STYLE_ASSIGNMENT((#44208));
ENDSEC;
END-ISO-10303-21;
